ISO-10303-21;
HEADER;
FILE_DESCRIPTION((''),'2;1');
FILE_NAME('HUB_LOCK_NUT_M10.step','2026-10-01T22:05:39-07:00',(''),(''),'','','');
FILE_SCHEMA (('AUTOMOTIVE_DESIGN { 1 0 10303 214 3 1 1 }'));
ENDSEC;
DATA;
#10=MECHANICAL_DESIGN_GEOMETRIC_PRESENTATION_REPRESENTATION('',(#643),#24628);
#559=SHAPE_REPRESENTATION_RELATIONSHIP('SRR','None',#24834,#601) ;
#601=ADVANCED_BREP_SHAPE_REPRESENTATION('',(#682),#24624) ;
#643=STYLED_ITEM('',(#25030),#682) ;
#682=MANIFOLD_SOLID_BREP('HUB_LOCK_NUT_M10',#13185) ;
#945=FACE_BOUND('',#4711,.T.) ;
#946=FACE_BOUND('',#4717,.T.) ;
#1761=LINE('',#24333,#2597) ;
#1762=LINE('',#24338,#2598) ;
#1763=LINE('',#24340,#2599) ;
#1764=LINE('',#24342,#2600) ;
#1765=LINE('',#24343,#2601) ;
#1766=LINE('',#24347,#2602) ;
#1767=LINE('',#24349,#2603) ;
#1768=LINE('',#24351,#2604) ;
#1769=LINE('',#24352,#2605) ;
#1770=LINE('',#24355,#2606) ;
#1771=LINE('',#24356,#2607) ;
#1772=LINE('',#24358,#2608) ;
#1773=LINE('',#24359,#2609) ;
#1774=LINE('',#24362,#2610) ;
#1775=LINE('',#24363,#2611) ;
#1776=LINE('',#24366,#2612) ;
#1777=LINE('',#24367,#2613) ;
#1778=LINE('',#24369,#2614) ;
#1779=LINE('',#24371,#2615) ;
#2597=VECTOR('',#19486,0.5) ;
#2598=VECTOR('',#19491,1.) ;
#2599=VECTOR('',#19492,1.) ;
#2600=VECTOR('',#19493,1.) ;
#2601=VECTOR('',#19494,1.) ;
#2602=VECTOR('',#19497,1.) ;
#2603=VECTOR('',#19498,1.) ;
#2604=VECTOR('',#19499,1.) ;
#2605=VECTOR('',#19500,1.) ;
#2606=VECTOR('',#19503,1.) ;
#2607=VECTOR('',#19504,1.) ;
#2608=VECTOR('',#19505,1.) ;
#2609=VECTOR('',#19506,1.) ;
#2610=VECTOR('',#19509,1.) ;
#2611=VECTOR('',#19510,1.) ;
#2612=VECTOR('',#19513,1.) ;
#2613=VECTOR('',#19514,1.) ;
#2614=VECTOR('',#19517,1.) ;
#2615=VECTOR('',#19520,1.) ;
#2948=CYLINDRICAL_SURFACE('',#15318,0.5) ;
#3681=FACE_OUTER_BOUND('',#4707,.T.) ;
#3682=FACE_OUTER_BOUND('',#4708,.T.) ;
#3683=FACE_OUTER_BOUND('',#4709,.T.) ;
#3684=FACE_OUTER_BOUND('',#4710,.T.) ;
#3685=FACE_OUTER_BOUND('',#4712,.T.) ;
#3686=FACE_OUTER_BOUND('',#4713,.T.) ;
#3687=FACE_OUTER_BOUND('',#4714,.T.) ;
#3688=FACE_OUTER_BOUND('',#4715,.T.) ;
#3689=FACE_OUTER_BOUND('',#4716,.T.) ;
#4707=EDGE_LOOP('',(#11827,#11828,#11829,#11830)) ;
#4708=EDGE_LOOP('',(#11831,#11832,#11833,#11834)) ;
#4709=EDGE_LOOP('',(#11835,#11836,#11837,#11838)) ;
#4710=EDGE_LOOP('',(#11839,#11840,#11841,#11842,#11843,#11844)) ;
#4711=EDGE_LOOP('',(#11845)) ;
#4712=EDGE_LOOP('',(#11846,#11847,#11848,#11849)) ;
#4713=EDGE_LOOP('',(#11850,#11851,#11852,#11853)) ;
#4714=EDGE_LOOP('',(#11854,#11855,#11856,#11857)) ;
#4715=EDGE_LOOP('',(#11858,#11859,#11860,#11861)) ;
#4716=EDGE_LOOP('',(#11862,#11863,#11864,#11865,#11866,#11867)) ;
#4717=EDGE_LOOP('',(#11868)) ;
#5529=CIRCLE('',#15319,0.5) ;
#5530=CIRCLE('',#15320,0.5) ;
#6677=VERTEX_POINT('',#24330) ;
#6678=VERTEX_POINT('',#24332) ;
#6679=VERTEX_POINT('',#24336) ;
#6680=VERTEX_POINT('',#24337) ;
#6681=VERTEX_POINT('',#24339) ;
#6682=VERTEX_POINT('',#24341) ;
#6683=VERTEX_POINT('',#24345) ;
#6684=VERTEX_POINT('',#24346) ;
#6685=VERTEX_POINT('',#24348) ;
#6686=VERTEX_POINT('',#24350) ;
#6687=VERTEX_POINT('',#24354) ;
#6688=VERTEX_POINT('',#24357) ;
#6689=VERTEX_POINT('',#24361) ;
#6690=VERTEX_POINT('',#24365) ;
#8403=EDGE_CURVE('',#6677,#6677,#5529,.T.) ;
#8404=EDGE_CURVE('',#6677,#6678,#1761,.T.) ;
#8405=EDGE_CURVE('',#6678,#6678,#5530,.T.) ;
#8406=EDGE_CURVE('',#6679,#6680,#1762,.T.) ;
#8407=EDGE_CURVE('',#6679,#6681,#1763,.T.) ;
#8408=EDGE_CURVE('',#6682,#6681,#1764,.T.) ;
#8409=EDGE_CURVE('',#6682,#6680,#1765,.T.) ;
#8410=EDGE_CURVE('',#6683,#6684,#1766,.T.) ;
#8411=EDGE_CURVE('',#6683,#6685,#1767,.T.) ;
#8412=EDGE_CURVE('',#6686,#6685,#1768,.T.) ;
#8413=EDGE_CURVE('',#6686,#6684,#1769,.T.) ;
#8414=EDGE_CURVE('',#6687,#6679,#1770,.T.) ;
#8415=EDGE_CURVE('',#6685,#6687,#1771,.T.) ;
#8416=EDGE_CURVE('',#6688,#6683,#1772,.T.) ;
#8417=EDGE_CURVE('',#6681,#6688,#1773,.T.) ;
#8418=EDGE_CURVE('',#6687,#6689,#1774,.T.) ;
#8419=EDGE_CURVE('',#6680,#6689,#1775,.T.) ;
#8420=EDGE_CURVE('',#6688,#6690,#1776,.T.) ;
#8421=EDGE_CURVE('',#6684,#6690,#1777,.T.) ;
#8422=EDGE_CURVE('',#6689,#6686,#1778,.T.) ;
#8423=EDGE_CURVE('',#6690,#6682,#1779,.T.) ;
#11827=ORIENTED_EDGE('',*,*,#8403,.F.) ;
#11828=ORIENTED_EDGE('',*,*,#8404,.T.) ;
#11829=ORIENTED_EDGE('',*,*,#8405,.F.) ;
#11830=ORIENTED_EDGE('',*,*,#8404,.F.) ;
#11831=ORIENTED_EDGE('',*,*,#8406,.F.) ;
#11832=ORIENTED_EDGE('',*,*,#8407,.T.) ;
#11833=ORIENTED_EDGE('',*,*,#8408,.F.) ;
#11834=ORIENTED_EDGE('',*,*,#8409,.T.) ;
#11835=ORIENTED_EDGE('',*,*,#8410,.F.) ;
#11836=ORIENTED_EDGE('',*,*,#8411,.T.) ;
#11837=ORIENTED_EDGE('',*,*,#8412,.F.) ;
#11838=ORIENTED_EDGE('',*,*,#8413,.T.) ;
#11839=ORIENTED_EDGE('',*,*,#8407,.F.) ;
#11840=ORIENTED_EDGE('',*,*,#8414,.F.) ;
#11841=ORIENTED_EDGE('',*,*,#8415,.F.) ;
#11842=ORIENTED_EDGE('',*,*,#8411,.F.) ;
#11843=ORIENTED_EDGE('',*,*,#8416,.F.) ;
#11844=ORIENTED_EDGE('',*,*,#8417,.F.) ;
#11845=ORIENTED_EDGE('',*,*,#8403,.T.) ;
#11846=ORIENTED_EDGE('',*,*,#8418,.F.) ;
#11847=ORIENTED_EDGE('',*,*,#8414,.T.) ;
#11848=ORIENTED_EDGE('',*,*,#8406,.T.) ;
#11849=ORIENTED_EDGE('',*,*,#8419,.T.) ;
#11850=ORIENTED_EDGE('',*,*,#8420,.F.) ;
#11851=ORIENTED_EDGE('',*,*,#8416,.T.) ;
#11852=ORIENTED_EDGE('',*,*,#8410,.T.) ;
#11853=ORIENTED_EDGE('',*,*,#8421,.T.) ;
#11854=ORIENTED_EDGE('',*,*,#8418,.T.) ;
#11855=ORIENTED_EDGE('',*,*,#8422,.T.) ;
#11856=ORIENTED_EDGE('',*,*,#8412,.T.) ;
#11857=ORIENTED_EDGE('',*,*,#8415,.T.) ;
#11858=ORIENTED_EDGE('',*,*,#8408,.T.) ;
#11859=ORIENTED_EDGE('',*,*,#8417,.T.) ;
#11860=ORIENTED_EDGE('',*,*,#8420,.T.) ;
#11861=ORIENTED_EDGE('',*,*,#8423,.T.) ;
#11862=ORIENTED_EDGE('',*,*,#8409,.F.) ;
#11863=ORIENTED_EDGE('',*,*,#8423,.F.) ;
#11864=ORIENTED_EDGE('',*,*,#8421,.F.) ;
#11865=ORIENTED_EDGE('',*,*,#8413,.F.) ;
#11866=ORIENTED_EDGE('',*,*,#8422,.F.) ;
#11867=ORIENTED_EDGE('',*,*,#8419,.F.) ;
#11868=ORIENTED_EDGE('',*,*,#8405,.T.) ;
#12313=PLANE('',#15321) ;
#12314=PLANE('',#15322) ;
#12315=PLANE('',#15323) ;
#12316=PLANE('',#15324) ;
#12317=PLANE('',#15325) ;
#12318=PLANE('',#15326) ;
#12319=PLANE('',#15327) ;
#12320=PLANE('',#15328) ;
#13076=ADVANCED_FACE('',(#3681),#2948,.F.) ;
#13077=ADVANCED_FACE('',(#3682),#12313,.F.) ;
#13078=ADVANCED_FACE('',(#3683),#12314,.F.) ;
#13079=ADVANCED_FACE('',(#3684,#945),#12315,.T.) ;
#13080=ADVANCED_FACE('',(#3685),#12316,.F.) ;
#13081=ADVANCED_FACE('',(#3686),#12317,.F.) ;
#13082=ADVANCED_FACE('',(#3687),#12318,.F.) ;
#13083=ADVANCED_FACE('',(#3688),#12319,.F.) ;
#13084=ADVANCED_FACE('',(#3689,#946),#12320,.T.) ;
#13185=CLOSED_SHELL('',(#13076,#13077,#13078,#13079,#13080,#13081,#13082,
#13083,#13084)) ;
#15317=AXIS2_PLACEMENT_3D('',#24328,#19480,#19481) ;
#15318=AXIS2_PLACEMENT_3D('',#24329,#19482,#19483) ;
#15319=AXIS2_PLACEMENT_3D('',#24331,#19484,#19485) ;
#15320=AXIS2_PLACEMENT_3D('',#24334,#19487,#19488) ;
#15321=AXIS2_PLACEMENT_3D('',#24335,#19489,#19490) ;
#15322=AXIS2_PLACEMENT_3D('',#24344,#19495,#19496) ;
#15323=AXIS2_PLACEMENT_3D('',#24353,#19501,#19502) ;
#15324=AXIS2_PLACEMENT_3D('',#24360,#19507,#19508) ;
#15325=AXIS2_PLACEMENT_3D('',#24364,#19511,#19512) ;
#15326=AXIS2_PLACEMENT_3D('',#24368,#19515,#19516) ;
#15327=AXIS2_PLACEMENT_3D('',#24370,#19518,#19519) ;
#15328=AXIS2_PLACEMENT_3D('',#24372,#19521,#19522) ;
#19480=DIRECTION('axis',(0.,0.,1.)) ;
#19481=DIRECTION('refdir',(1.,0.,0.)) ;
#19482=DIRECTION('center_axis',(0.,1.,0.)) ;
#19483=DIRECTION('ref_axis',(1.,0.,0.)) ;
#19484=DIRECTION('center_axis',(0.,1.,0.)) ;
#19485=DIRECTION('ref_axis',(1.,0.,0.)) ;
#19486=DIRECTION('',(0.,1.,0.)) ;
#19487=DIRECTION('center_axis',(0.,-1.,0.)) ;
#19488=DIRECTION('ref_axis',(1.,0.,0.)) ;
#19489=DIRECTION('center_axis',(-0.5,0.,-0.866025403784439)) ;
#19490=DIRECTION('ref_axis',(-0.866025403784439,0.,0.5)) ;
#19491=DIRECTION('',(0.,1.,0.)) ;
#19492=DIRECTION('',(0.866025403784439,0.,-0.5)) ;
#19493=DIRECTION('',(0.,-1.,0.)) ;
#19494=DIRECTION('',(-0.866025403784439,0.,0.5)) ;
#19495=DIRECTION('center_axis',(0.5,0.,0.866025403784439)) ;
#19496=DIRECTION('ref_axis',(0.866025403784439,0.,-0.5)) ;
#19497=DIRECTION('',(0.,1.,0.)) ;
#19498=DIRECTION('',(-0.866025403784439,0.,0.5)) ;
#19499=DIRECTION('',(0.,-1.,0.)) ;
#19500=DIRECTION('',(0.866025403784439,0.,-0.5)) ;
#19501=DIRECTION('center_axis',(0.,-1.,0.)) ;
#19502=DIRECTION('ref_axis',(-1.,0.,0.)) ;
#19503=DIRECTION('',(0.866025403784439,0.,0.5)) ;
#19504=DIRECTION('',(0.,0.,1.)) ;
#19505=DIRECTION('',(-0.866025403784439,0.,-0.5)) ;
#19506=DIRECTION('',(0.,0.,-1.)) ;
#19507=DIRECTION('center_axis',(0.5,0.,-0.866025403784439)) ;
#19508=DIRECTION('ref_axis',(-0.866025403784439,0.,-0.5)) ;
#19509=DIRECTION('',(0.,1.,0.)) ;
#19510=DIRECTION('',(-0.866025403784439,0.,-0.5)) ;
#19511=DIRECTION('center_axis',(-0.5,0.,0.866025403784439)) ;
#19512=DIRECTION('ref_axis',(0.866025403784439,0.,0.5)) ;
#19513=DIRECTION('',(0.,1.,0.)) ;
#19514=DIRECTION('',(0.866025403784439,0.,0.5)) ;
#19515=DIRECTION('center_axis',(1.,0.,0.)) ;
#19516=DIRECTION('ref_axis',(0.,0.,-1.)) ;
#19517=DIRECTION('',(0.,0.,-1.)) ;
#19518=DIRECTION('center_axis',(-1.,0.,0.)) ;
#19519=DIRECTION('ref_axis',(0.,0.,1.)) ;
#19520=DIRECTION('',(0.,0.,1.)) ;
#19521=DIRECTION('center_axis',(0.,1.,0.)) ;
#19522=DIRECTION('ref_axis',(1.,0.,0.)) ;
#24328=CARTESIAN_POINT('',(0.,0.,0.)) ;
#24329=CARTESIAN_POINT('Origin',(0.,0.3,0.)) ;
#24330=CARTESIAN_POINT('',(-0.5,-0.1,6.12323399573677E-17)) ;
#24331=CARTESIAN_POINT('Origin',(0.,-0.1,0.)) ;
#24332=CARTESIAN_POINT('',(-0.5,0.7,-6.12323399573677E-17)) ;
#24333=CARTESIAN_POINT('',(-0.5,0.3,6.12323399573677E-17)) ;
#24334=CARTESIAN_POINT('Origin',(0.,0.7,0.)) ;
#24335=CARTESIAN_POINT('Origin',(0.425,0.3,0.736121593216773)) ;
#24336=CARTESIAN_POINT('',(-3.33066907387547E-16,-0.1,0.981495457622364)) ;
#24337=CARTESIAN_POINT('',(-3.33066907387547E-16,0.7,0.981495457622364)) ;
#24338=CARTESIAN_POINT('',(-3.33066907387547E-16,0.3,0.981495457622364)) ;
#24339=CARTESIAN_POINT('',(0.85,-0.1,0.490747728811182)) ;
#24340=CARTESIAN_POINT('',(0.425,-0.1,0.736121593216773)) ;
#24341=CARTESIAN_POINT('',(0.85,0.7,0.490747728811182)) ;
#24342=CARTESIAN_POINT('',(0.85,0.3,0.490747728811182)) ;
#24343=CARTESIAN_POINT('',(0.425,0.7,0.736121593216773)) ;
#24344=CARTESIAN_POINT('Origin',(-0.425,0.3,-0.736121593216773)) ;
#24345=CARTESIAN_POINT('',(3.33066907387547E-16,-0.1,-0.981495457622364)) ;
#24346=CARTESIAN_POINT('',(3.33066907387547E-16,0.7,-0.981495457622364)) ;
#24347=CARTESIAN_POINT('',(3.33066907387547E-16,0.3,-0.981495457622364)) ;
#24348=CARTESIAN_POINT('',(-0.85,-0.1,-0.490747728811182)) ;
#24349=CARTESIAN_POINT('',(-0.425,-0.1,-0.736121593216773)) ;
#24350=CARTESIAN_POINT('',(-0.85,0.7,-0.490747728811182)) ;
#24351=CARTESIAN_POINT('',(-0.85,0.3,-0.490747728811182)) ;
#24352=CARTESIAN_POINT('',(-0.425,0.7,-0.736121593216773)) ;
#24353=CARTESIAN_POINT('Origin',(0.,-0.1,0.)) ;
#24354=CARTESIAN_POINT('',(-0.85,-0.1,0.490747728811182)) ;
#24355=CARTESIAN_POINT('',(-0.425,-0.1,0.736121593216773)) ;
#24356=CARTESIAN_POINT('',(-0.85,-0.1,0.)) ;
#24357=CARTESIAN_POINT('',(0.85,-0.1,-0.490747728811182)) ;
#24358=CARTESIAN_POINT('',(0.425,-0.1,-0.736121593216773)) ;
#24359=CARTESIAN_POINT('',(0.85,-0.1,0.)) ;
#24360=CARTESIAN_POINT('Origin',(-0.425,0.3,0.736121593216773)) ;
#24361=CARTESIAN_POINT('',(-0.85,0.7,0.490747728811182)) ;
#24362=CARTESIAN_POINT('',(-0.85,0.3,0.490747728811182)) ;
#24363=CARTESIAN_POINT('',(-0.425,0.7,0.736121593216773)) ;
#24364=CARTESIAN_POINT('Origin',(0.425,0.3,-0.736121593216773)) ;
#24365=CARTESIAN_POINT('',(0.85,0.7,-0.490747728811182)) ;
#24366=CARTESIAN_POINT('',(0.85,0.3,-0.490747728811182)) ;
#24367=CARTESIAN_POINT('',(0.425,0.7,-0.736121593216773)) ;
#24368=CARTESIAN_POINT('Origin',(-0.85,0.3,0.)) ;
#24369=CARTESIAN_POINT('',(-0.85,0.7,0.)) ;
#24370=CARTESIAN_POINT('Origin',(0.85,0.3,0.)) ;
#24371=CARTESIAN_POINT('',(0.85,0.7,0.)) ;
#24372=CARTESIAN_POINT('Origin',(0.,0.7,0.)) ;
#24576=UNCERTAINTY_MEASURE_WITH_UNIT(LENGTH_MEASURE(0.001),#24629,
'DISTANCE_ACCURACY_VALUE',
'Maximum model space distance between geometric entities at asserted c
onnectivities') ;
#24580=UNCERTAINTY_MEASURE_WITH_UNIT(LENGTH_MEASURE(0.001),#24629,
'DISTANCE_ACCURACY_VALUE',
'Maximum model space distance between geometric entities at asserted c
onnectivities') ;
#24624=(
GEOMETRIC_REPRESENTATION_CONTEXT(3)
GLOBAL_UNCERTAINTY_ASSIGNED_CONTEXT((#24576))
GLOBAL_UNIT_ASSIGNED_CONTEXT((#24629,#24631,#24632))
REPRESENTATION_CONTEXT('','3D')
) ;
#24628=(
GEOMETRIC_REPRESENTATION_CONTEXT(3)
GLOBAL_UNCERTAINTY_ASSIGNED_CONTEXT((#24580))
GLOBAL_UNIT_ASSIGNED_CONTEXT((#24629,#24631,#24632))
REPRESENTATION_CONTEXT('','3D')
) ;
#24629=(
LENGTH_UNIT()
NAMED_UNIT(*)
SI_UNIT(.CENTI.,.METRE.)
) ;
#24631=(
NAMED_UNIT(*)
PLANE_ANGLE_UNIT()
SI_UNIT($,.RADIAN.)
) ;
#24632=(
NAMED_UNIT(*)
SI_UNIT($,.STERADIAN.)
SOLID_ANGLE_UNIT()
) ;
#24676=SHAPE_DEFINITION_REPRESENTATION(#24764,#24834) ;
#24764=PRODUCT_DEFINITION_SHAPE('',$,#24882) ;
#24834=SHAPE_REPRESENTATION('',(#15317),#24624) ;
#24838=PRODUCT_DEFINITION_CONTEXT('part definition',#24981,'design') ;
#24882=PRODUCT_DEFINITION('HUB_LOCK_NUT_M10','HUB_LOCK_NUT_M10',
#24929,#24838) ;
#24929=PRODUCT_DEFINITION_FORMATION('',$,#25026) ;
#24981=APPLICATION_CONTEXT(
'Core Data for Automotive Mechanical Design Process') ;
#24982=PRODUCT_CONTEXT('part definition',#24981,'mechanical') ;
#25026=PRODUCT('HUB_LOCK_NUT_M10','HUB_LOCK_NUT_M10',$,(#24982)) ;
#25030=PRESENTATION_STYLE_ASSIGNMENT((#25040)) ;
#25040=SURFACE_STYLE_USAGE(.BOTH.,#25050) ;
#25050=SURFACE_SIDE_STYLE('',(#25060)) ;
#25060=SURFACE_STYLE_FILL_AREA(#25070) ;
#25070=FILL_AREA_STYLE('Steel - Satin',(#25080)) ;
#25080=FILL_AREA_STYLE_COLOUR('Steel - Satin',#25090) ;
#25090=COLOUR_RGB('Steel - Satin', 0.66274510, 0.83137255, 0.94901961) ;
ENDSEC;
END-ISO-10303-21;
